ISO-10303-21;
HEADER;
FILE_DESCRIPTION (('STEP AP214'),
    '1' );
FILE_NAME ('Flange.step',
    '2026-10-07T17:53:07',
    ( '' ),
    ( '' ),
    'SwSTEP 2.0',
    'SolidWorks 2025',
    '' );
FILE_SCHEMA (( 'AUTOMOTIVE_DESIGN' ));
ENDSEC;

DATA;
#2=VERTEX_POINT ( 'NONE', #7279 ) ;
#7=CARTESIAN_POINT ( 'NONE',  ( -0.04028432657539327000, 0.000000000000000000, 20.54539866546728533 ) ) ;
#31=DIRECTION ( 'NONE',  ( -0.000000000000000000, 1.000000000000000000, -0.000000000000000000 ) ) ;
#43=DIRECTION ( 'NONE',  ( 0.000000000000000000, 1.000000000000000000, 0.000000000000000000 ) ) ;
#66=EDGE_CURVE ( 'NONE', #2, #10148, #3731, .T. ) ;
#76=AXIS2_PLACEMENT_3D ( 'NONE', #7169, #9139, #1729 ) ;
#79=EDGE_LOOP ( 'NONE', ( #3659, #11191, #12245, #181 ) ) ;
#91=CARTESIAN_POINT ( 'NONE',  ( 7.347880794884120722E-16, 0.000000000000000000, -6.000000000000000888 ) ) ;
#99=DIRECTION ( 'NONE',  ( 0.000000000000000000, 0.000000000000000000, 1.000000000000000000 ) ) ;
#115=EDGE_LOOP ( 'NONE', ( #6121, #285 ) ) ;
#172=VERTEX_POINT ( 'NONE', #11643 ) ;
#179=VECTOR ( 'NONE', #6554, 1000.000000000000000 ) ;
#181=ORIENTED_EDGE ( 'NONE', *, *, #4608, .T. ) ;
#263=EDGE_CURVE ( 'NONE', #9409, #2919, #1933, .T. ) ;
#276=FACE_BOUND ( 'NONE', #615, .T. ) ;
#285=ORIENTED_EDGE ( 'NONE', *, *, #12452, .F. ) ;
#301=EDGE_LOOP ( 'NONE', ( #4662, #10708, #11788, #11819 ) ) ;
#315=EDGE_CURVE ( 'NONE', #6783, #8119, #5237, .T. ) ;
#327=LINE ( 'NONE', #1436, #6881 ) ;
#333=CARTESIAN_POINT ( 'NONE',  ( 4.599650328638321461, 8.500000000000001776, 5.878124499050803919 ) ) ;
#336=DIRECTION ( 'NONE',  ( -0.000000000000000000, 1.000000000000000000, -0.000000000000000000 ) ) ;
#338=CYLINDRICAL_SURFACE ( 'NONE', #13333, 6.000000000000000888 ) ;
#344=DIRECTION ( 'NONE',  ( -0.000000000000000000, 1.000000000000000000, -0.000000000000000000 ) ) ;
#377=ORIENTED_EDGE ( 'NONE', *, *, #5510, .F. ) ;
#380=VERTEX_POINT ( 'NONE', #1045 ) ;
#399=CARTESIAN_POINT ( 'NONE',  ( 4.599650328638321461, 8.500000000000000000, 7.878124499050794149 ) ) ;
#400=EDGE_CURVE ( 'NONE', #2628, #8206, #6299, .T. ) ;
#402=FACE_OUTER_BOUND ( 'NONE', #1652, .T. ) ;
#413=CIRCLE ( 'NONE', #2654, 1.999999999999994893 ) ;
#424=SURFACE_SIDE_STYLE ('',( #6838 ) ) ;
#433=ORIENTED_EDGE ( 'NONE', *, *, #4646, .T. ) ;
#436=ORIENTED_EDGE ( 'NONE', *, *, #2415, .T. ) ;
#440=DIRECTION ( 'NONE',  ( -0.000000000000000000, 1.000000000000000000, -0.000000000000000000 ) ) ;
#452=ORIENTED_EDGE ( 'NONE', *, *, #263, .F. ) ;
#459=CARTESIAN_POINT ( 'NONE',  ( -4.599650328638321461, 8.500000000000001776, -7.878124499050794149 ) ) ;
#479=CARTESIAN_POINT ( 'NONE',  ( 0.000000000000000000, -17.50000000000000000, 0.000000000000000000 ) ) ;
#481=FACE_BOUND ( 'NONE', #4546, .T. ) ;
#486=( GEOMETRIC_REPRESENTATION_CONTEXT ( 3 ) GLOBAL_UNCERTAINTY_ASSIGNED_CONTEXT ( ( #1243 ) ) GLOBAL_UNIT_ASSIGNED_CONTEXT ( ( #3583, #2756, #11179 ) ) REPRESENTATION_CONTEXT ( 'NONE', 'WORKASPACE' ) );
#499=FILL_AREA_STYLE_COLOUR ( '', #7596 ) ;
#507=EDGE_CURVE ( 'NONE', #12691, #7299, #11644, .T. ) ;
#539=FACE_OUTER_BOUND ( 'NONE', #11404, .T. ) ;
#541=DIRECTION ( 'NONE',  ( -0.000000000000000000, -1.000000000000000000, -0.000000000000000000 ) ) ;
#555=FACE_BOUND ( 'NONE', #11070, .T. ) ;
#556=SURFACE_STYLE_USAGE ( .BOTH. , #424 ) ;
#565=CLOSED_SHELL ( 'NONE', ( #6640, #3677, #5018, #11103, #4713, #11376, #9347, #11175, #12290, #2468, #10794, #12497, #7213, #4834, #4033, #591, #10301, #3376, #8262, #6490, #6495, #4028, #2671, #2050, #11073 ) ) ;
#573=EDGE_LOOP ( 'NONE', ( #4000, #4344 ) ) ;
#580=ORIENTED_EDGE ( 'NONE', *, *, #4518, .F. ) ;
#591=ADVANCED_FACE ( 'NONE', ( #11178, #689, #555, #1466 ), #9995, .T. ) ;
#595=CARTESIAN_POINT ( 'NONE',  ( 0.000000000000000000, 8.500000000000000000, 0.000000000000000000 ) ) ;
#615=EDGE_LOOP ( 'NONE', ( #433, #3515 ) ) ;
#621=DIRECTION ( 'NONE',  ( -0.000000000000000000, 1.000000000000000000, -0.000000000000000000 ) ) ;
#624=DIRECTION ( 'NONE',  ( 0.000000000000000000, 0.000000000000000000, 1.000000000000000000 ) ) ;
#662=EDGE_CURVE ( 'NONE', #12520, #2653, #11388, .T. ) ;
#689=FACE_BOUND ( 'NONE', #573, .T. ) ;
#696=DIRECTION ( 'NONE',  ( 0.000000000000000000, 0.000000000000000000, 1.000000000000000000 ) ) ;
#699=ORIENTED_EDGE ( 'NONE', *, *, #2777, .F. ) ;
#716=AXIS2_PLACEMENT_3D ( 'NONE', #8147, #3761, #12356 ) ;
#724=EDGE_LOOP ( 'NONE', ( #8738, #2157, #10866, #9680 ) ) ;
#738=PRODUCT_DEFINITION ( 'UNKNOWN', '', #8446, #5982 ) ;
#746=DIRECTION ( 'NONE',  ( 0.000000000000000000, -0.000000000000000000, 1.000000000000000000 ) ) ;
#780=DIRECTION ( 'NONE',  ( -0.000000000000000000, 1.000000000000000000, -0.000000000000000000 ) ) ;
#785=DIRECTION ( 'NONE',  ( 0.000000000000000000, 0.000000000000000000, 1.000000000000000000 ) ) ;
#809=DIRECTION ( 'NONE',  ( -0.000000000000000000, -1.000000000000000000, -0.000000000000000000 ) ) ;
#820=EDGE_CURVE ( 'NONE', #10863, #8191, #7815, .T. ) ;
#823=DIRECTION ( 'NONE',  ( 0.000000000000000000, 0.000000000000000000, 1.000000000000000000 ) ) ;
#859=VERTEX_POINT ( 'NONE', #5564 ) ;
#861=CIRCLE ( 'NONE', #5312, 13.50000000000000000 ) ;
#869=CARTESIAN_POINT ( 'NONE',  ( 0.04028432657539351286, 4.500000000000000000, -20.54539866546728888 ) ) ;
#920=DIRECTION ( 'NONE',  ( 0.000000000000000000, 0.000000000000000000, 1.000000000000000000 ) ) ;
#978=DIRECTION ( 'NONE',  ( 0.000000000000000000, 0.000000000000000000, 1.000000000000000000 ) ) ;
#985=EDGE_LOOP ( 'NONE', ( #2986, #6545, #13641, #7697 ) ) ;
#997=VERTEX_POINT ( 'NONE', #7721 ) ;
#1006=DIRECTION ( 'NONE',  ( 0.000000000000000000, 1.000000000000000000, 0.000000000000000000 ) ) ;
#1011=ORIENTED_EDGE ( 'NONE', *, *, #12563, .F. ) ;
#1045=CARTESIAN_POINT ( 'NONE',  ( 16.04064420431708982, 0.000000000000000000, 7.307586582922145801 ) ) ;
#1087=DIRECTION ( 'NONE',  ( 0.000000000000000000, 0.000000000000000000, 1.000000000000000000 ) ) ;
#1116=AXIS2_PLACEMENT_3D ( 'NONE', #7517, #1325, #3440 ) ;
#1243=UNCERTAINTY_MEASURE_WITH_UNIT (LENGTH_MEASURE( 1.000000000000000082E-05 ), #3583, 'distance_accuracy_value', 'NONE');
#1277=ORIENTED_EDGE ( 'NONE', *, *, #10649, .F. ) ;
#1286=EDGE_CURVE ( 'NONE', #9471, #9880, #10745, .T. ) ;
#1307=FACE_OUTER_BOUND ( 'NONE', #9354, .T. ) ;
#1309=FACE_BOUND ( 'NONE', #7385, .T. ) ;
#1325=DIRECTION ( 'NONE',  ( 0.000000000000000000, 1.000000000000000000, 0.000000000000000000 ) ) ;
#1327=ORIENTED_EDGE ( 'NONE', *, *, #11562, .T. ) ;
#1339=EDGE_LOOP ( 'NONE', ( #5946, #3463 ) ) ;
#1353=EDGE_CURVE ( 'NONE', #12408, #9471, #4156, .T. ) ;
#1362=DIRECTION ( 'NONE',  ( -0.000000000000000000, 1.000000000000000000, -0.000000000000000000 ) ) ;
#1363=ORIENTED_EDGE ( 'NONE', *, *, #662, .F. ) ;
#1376=AXIS2_PLACEMENT_3D ( 'NONE', #4675, #11938, #2530 ) ;
#1384=DIRECTION ( 'NONE',  ( -0.000000000000000000, 1.000000000000000000, -0.000000000000000000 ) ) ;
#1421=DIRECTION ( 'NONE',  ( 0.000000000000000000, 0.000000000000000000, 1.000000000000000000 ) ) ;
#1424=CARTESIAN_POINT ( 'NONE',  ( -4.599650328638321461, 0.000000000000000000, -5.878124499050807472 ) ) ;
#1425=EDGE_LOOP ( 'NONE', ( #8670, #4151, #1327, #8418 ) ) ;
#1429=ORIENTED_EDGE ( 'NONE', *, *, #4536, .F. ) ;
#1430=ORIENTED_EDGE ( 'NONE', *, *, #10166, .F. ) ;
#1436=CARTESIAN_POINT ( 'NONE',  ( 16.04064420431708982, 4.500000000000000000, 11.30758658292212893 ) ) ;
#1466=FACE_OUTER_BOUND ( 'NONE', #7959, .T. ) ;
#1470=FACE_BOUND ( 'NONE', #9238, .T. ) ;
#1564=AXIS2_PLACEMENT_3D ( 'NONE', #13614, #12313, #696 ) ;
#1580=AXIS2_PLACEMENT_3D ( 'NONE', #8151, #5909, #3640 ) ;
#1602=EDGE_CURVE ( 'NONE', #11352, #997, #3845, .T. ) ;
#1626=DIRECTION ( 'NONE',  ( -0.000000000000000000, 1.000000000000000000, -0.000000000000000000 ) ) ;
#1652=EDGE_LOOP ( 'NONE', ( #10510, #6611, #2690, #10999 ) ) ;
#1662=DIRECTION ( 'NONE',  ( 0.000000000000000000, 0.000000000000000000, 1.000000000000000000 ) ) ;
#1675=CARTESIAN_POINT ( 'NONE',  ( 0.000000000000000000, 8.500000000000000000, 0.000000000000000000 ) ) ;
#1694=DIRECTION ( 'NONE',  ( -0.000000000000000000, 1.000000000000000000, -0.000000000000000000 ) ) ;
#1709=CARTESIAN_POINT ( 'NONE',  ( -0.04028432657539327000, 4.500000000000000000, 18.54539866546729243 ) ) ;
#1729=DIRECTION ( 'NONE',  ( 0.000000000000000000, 0.000000000000000000, 1.000000000000000000 ) ) ;
#1751=DIRECTION ( 'NONE',  ( 0.000000000000000000, 1.000000000000000000, 0.000000000000000000 ) ) ;
#1765=ORIENTED_EDGE ( 'NONE', *, *, #8460, .F. ) ;
#1776=CIRCLE ( 'NONE', #2234, 1.999999999999991340 ) ;
#1790=EDGE_CURVE ( 'NONE', #13129, #13550, #2981, .T. ) ;
#1791=DIRECTION ( 'NONE',  ( -0.000000000000000000, 1.000000000000000000, -0.000000000000000000 ) ) ;
#1803=AXIS2_PLACEMENT_3D ( 'NONE', #4818, #4693, #10276 ) ;
#1814=AXIS2_PLACEMENT_3D ( 'NONE', #5408, #6257, #99 ) ;
#1849=ORIENTED_EDGE ( 'NONE', *, *, #4848, .F. ) ;
#1862=CYLINDRICAL_SURFACE ( 'NONE', #3130, 1.999999999999991340 ) ;
#1873=CIRCLE ( 'NONE', #76, 23.49999999999999645 ) ;
#1922=CARTESIAN_POINT ( 'NONE',  ( 4.599650328638321461, 0.000000000000000000, 9.878124499050780827 ) ) ;
#1933=CIRCLE ( 'NONE', #3717, 1.999999999999994893 ) ;
#1949=EDGE_CURVE ( 'NONE', #10148, #2653, #6694, .T. ) ;
#1975=AXIS2_PLACEMENT_3D ( 'NONE', #5600, #11899, #2421 ) ;
#1994=ORIENTED_EDGE ( 'NONE', *, *, #9182, .F. ) ;
#1996=ORIENTED_EDGE ( 'NONE', *, *, #7403, .F. ) ;
#2027=FACE_OUTER_BOUND ( 'NONE', #12665, .T. ) ;
#2029=CARTESIAN_POINT ( 'NONE',  ( 16.04064420431708982, 0.000000000000000000, 11.30758658292212893 ) ) ;
#2050=ADVANCED_FACE ( 'NONE', ( #11238 ), #4679, .F. ) ;
#2083=CIRCLE ( 'NONE', #10773, 1.999999999999994893 ) ;
#2145=CYLINDRICAL_SURFACE ( 'NONE', #3565, 6.000000000000000888 ) ;
#2149=VERTEX_POINT ( 'NONE', #2029 ) ;
#2157=ORIENTED_EDGE ( 'NONE', *, *, #3698, .T. ) ;
#2174=CYLINDRICAL_SURFACE ( 'NONE', #11564, 1.999999999999991340 ) ;
#2206=LINE ( 'NONE', #9670, #6872 ) ;
#2212=DIRECTION ( 'NONE',  ( 0.000000000000000000, 0.000000000000000000, 1.000000000000000000 ) ) ;
#2234=AXIS2_PLACEMENT_3D ( 'NONE', #13029, #3474, #9620 ) ;
#2292=EDGE_LOOP ( 'NONE', ( #580, #3180, #12636, #7033 ) ) ;
#2295=ORIENTED_EDGE ( 'NONE', *, *, #6049, .T. ) ;
#2320=AXIS2_PLACEMENT_3D ( 'NONE', #8544, #9673, #7465 ) ;
#2332=ORIENTED_EDGE ( 'NONE', *, *, #9772, .F. ) ;
#2341=DIRECTION ( 'NONE',  ( 0.000000000000000000, -0.000000000000000000, 1.000000000000000000 ) ) ;
#2342=EDGE_CURVE ( 'NONE', #172, #6605, #2501, .T. ) ;
#2351=FACE_OUTER_BOUND ( 'NONE', #5450, .T. ) ;
#2357=LINE ( 'NONE', #4431, #4938 ) ;
#2396=DIRECTION ( 'NONE',  ( -0.000000000000000000, 1.000000000000000000, -0.000000000000000000 ) ) ;
#2415=EDGE_CURVE ( 'NONE', #6705, #5000, #2646, .T. ) ;
#2419=VECTOR ( 'NONE', #12619, 1000.000000000000000 ) ;
#2421=DIRECTION ( 'NONE',  ( 0.000000000000000000, 0.000000000000000000, 1.000000000000000000 ) ) ;
#2435=VECTOR ( 'NONE', #2396, 1000.000000000000000 ) ;
#2440=CIRCLE ( 'NONE', #12010, 1.999999999999994893 ) ;
#2442=CARTESIAN_POINT ( 'NONE',  ( -16.08092853089235774, 4.500000000000000000, 7.237812082545092451 ) ) ;
#2454=CARTESIAN_POINT ( 'NONE',  ( 1.653273178848926867E-15, 8.500000000000000000, 13.50000000000000000 ) ) ;
#2463=DIRECTION ( 'NONE',  ( 0.000000000000000000, 0.000000000000000000, 1.000000000000000000 ) ) ;
#2468=ADVANCED_FACE ( 'NONE', ( #6876 ), #7853, .T. ) ;
#2475=DIRECTION ( 'NONE',  ( -0.000000000000000000, 1.000000000000000000, -0.000000000000000000 ) ) ;
#2501=CIRCLE ( 'NONE', #6038, 23.49999999999999645 ) ;
#2522=DIRECTION ( 'NONE',  ( -0.000000000000000000, 1.000000000000000000, -0.000000000000000000 ) ) ;
#2526=LINE ( 'NONE', #11093, #8476 ) ;
#2530=DIRECTION ( 'NONE',  ( 0.000000000000000000, 0.000000000000000000, 1.000000000000000000 ) ) ;
#2532=DIRECTION ( 'NONE',  ( 0.000000000000000000, 1.000000000000000000, 0.000000000000000000 ) ) ;
#2562=DIRECTION ( 'NONE',  ( 0.000000000000000000, 0.000000000000000000, 1.000000000000000000 ) ) ;
#2576=DIRECTION ( 'NONE',  ( -0.000000000000000000, 1.000000000000000000, -0.000000000000000000 ) ) ;
#2579=DIRECTION ( 'NONE',  ( -0.000000000000000000, -1.000000000000000000, -0.000000000000000000 ) ) ;
#2627=CARTESIAN_POINT ( 'NONE',  ( -16.04064420431702942, 4.500000000000000000, -9.307586582922249718 ) ) ;
#2628=VERTEX_POINT ( 'NONE', #10310 ) ;
#2645=DIRECTION ( 'NONE',  ( -0.000000000000000000, 1.000000000000000000, -0.000000000000000000 ) ) ;
#2646=LINE ( 'NONE', #3622, #2951 ) ;
#2653=VERTEX_POINT ( 'NONE', #869 ) ;
#2654=AXIS2_PLACEMENT_3D ( 'NONE', #9886, #440, #8968 ) ;
#2662=FACE_BOUND ( 'NONE', #10571, .T. ) ;
#2671=ADVANCED_FACE ( 'NONE', ( #10516 ), #4027, .F. ) ;
#2690=ORIENTED_EDGE ( 'NONE', *, *, #10147, .T. ) ;
#2733=CARTESIAN_POINT ( 'NONE',  ( 0.000000000000000000, 0.000000000000000000, 0.000000000000000000 ) ) ;
#2756=( NAMED_UNIT ( * ) PLANE_ANGLE_UNIT ( ) SI_UNIT ( $, .RADIAN. ) );
#2757=DIRECTION ( 'NONE',  ( 0.000000000000000000, 1.000000000000000000, 0.000000000000000000 ) ) ;
#2777=EDGE_CURVE ( 'NONE', #11352, #5468, #2357, .T. ) ;
#2785=DIRECTION ( 'NONE',  ( -0.000000000000000000, 1.000000000000000000, -0.000000000000000000 ) ) ;
#2838=CARTESIAN_POINT ( 'NONE',  ( -16.04064420431702942, 4.500000000000000000, -9.307586582922249718 ) ) ;
#2845=EDGE_LOOP ( 'NONE', ( #452, #11261 ) ) ;
#2919=VERTEX_POINT ( 'NONE', #10160 ) ;
#2927=CARTESIAN_POINT ( 'NONE',  ( 16.04064420431708982, 4.500000000000000000, 9.307586582922137808 ) ) ;
#2944=DIRECTION ( 'NONE',  ( 0.000000000000000000, 0.000000000000000000, -1.000000000000000000 ) ) ;
#2951=VECTOR ( 'NONE', #10113, 1000.000000000000000 ) ;
#2954=DIRECTION ( 'NONE',  ( 0.000000000000000000, 1.000000000000000000, 0.000000000000000000 ) ) ;
#2964=CYLINDRICAL_SURFACE ( 'NONE', #1564, 1.999999999999991340 ) ;
#2981=LINE ( 'NONE', #8049, #8480 ) ;
#2984=CARTESIAN_POINT ( 'NONE',  ( -16.08092853089235774, 4.500000000000000000, 9.237812082545083570 ) ) ;
#2986=ORIENTED_EDGE ( 'NONE', *, *, #9366, .F. ) ;
#3006=DIRECTION ( 'NONE',  ( -0.000000000000000000, -1.000000000000000000, -0.000000000000000000 ) ) ;
#3011=CARTESIAN_POINT ( 'NONE',  ( 0.000000000000000000, 0.000000000000000000, 0.000000000000000000 ) ) ;
#3062=VERTEX_POINT ( 'NONE', #6085 ) ;
#3090=AXIS2_PLACEMENT_3D ( 'NONE', #7410, #1006, #2212 ) ;
#3130=AXIS2_PLACEMENT_3D ( 'NONE', #2927, #7077, #3747 ) ;
#3161=DIRECTION ( 'NONE',  ( 0.000000000000000000, 0.000000000000000000, 1.000000000000000000 ) ) ;
#3180=ORIENTED_EDGE ( 'NONE', *, *, #9472, .T. ) ;
#3182=DIRECTION ( 'NONE',  ( 0.000000000000000000, 0.000000000000000000, 1.000000000000000000 ) ) ;
#3186=CIRCLE ( 'NONE', #6286, 1.999999999999994893 ) ;
#3226=CARTESIAN_POINT ( 'NONE',  ( 0.04028432657539327000, 4.500000000000000000, -18.54539866546729243 ) ) ;
#3280=ORIENTED_EDGE ( 'NONE', *, *, #1286, .F. ) ;
#3285=CARTESIAN_POINT ( 'NONE',  ( -16.08092853089235774, 4.500000000000000000, 9.237812082545083570 ) ) ;
#3304=ORIENTED_EDGE ( 'NONE', *, *, #3666, .T. ) ;
#3324=CIRCLE ( 'NONE', #10252, 6.000000000000000888 ) ;
#3325=AXIS2_PLACEMENT_3D ( 'NONE', #459, #12130, #12055 ) ;
#3376=ADVANCED_FACE ( 'NONE', ( #9295 ), #2964, .F. ) ;
#3393=DIRECTION ( 'NONE',  ( -0.000000000000000000, 1.000000000000000000, -0.000000000000000000 ) ) ;
#3396=AXIS2_PLACEMENT_3D ( 'NONE', #11205, #11968, #1421 ) ;
#3420=VERTEX_POINT ( 'NONE', #6134 ) ;
#3440=DIRECTION ( 'NONE',  ( 0.000000000000000000, 0.000000000000000000, 1.000000000000000000 ) ) ;
#3463=ORIENTED_EDGE ( 'NONE', *, *, #9366, .T. ) ;
#3474=DIRECTION ( 'NONE',  ( 0.000000000000000000, 1.000000000000000000, 0.000000000000000000 ) ) ;
#3515=ORIENTED_EDGE ( 'NONE', *, *, #1602, .T. ) ;
#3563=DIRECTION ( 'NONE',  ( -0.000000000000000000, 1.000000000000000000, -0.000000000000000000 ) ) ;
#3565=AXIS2_PLACEMENT_3D ( 'NONE', #5328, #31, #10721 ) ;
#3566=FACE_OUTER_BOUND ( 'NONE', #7758, .T. ) ;
#3583=( LENGTH_UNIT ( ) NAMED_UNIT ( * ) SI_UNIT ( .MILLI., .METRE. ) );
#3593=VECTOR ( 'NONE', #7863, 1000.000000000000000 ) ;
#3622=CARTESIAN_POINT ( 'NONE',  ( 0.000000000000000000, -17.50000000000000000, 6.000000000000000888 ) ) ;
#3640=DIRECTION ( 'NONE',  ( 0.000000000000000000, 0.000000000000000000, 1.000000000000000000 ) ) ;
#3657=ORIENTED_EDGE ( 'NONE', *, *, #507, .F. ) ;
#3659=ORIENTED_EDGE ( 'NONE', *, *, #5188, .F. ) ;
#3666=EDGE_CURVE ( 'NONE', #11864, #9880, #2526, .T. ) ;
#3677=ADVANCED_FACE ( 'NONE', ( #9975 ), #11931, .F. ) ;
#3690=CYLINDRICAL_SURFACE ( 'NONE', #8881, 1.999999999999991340 ) ;
#3698=EDGE_CURVE ( 'NONE', #5985, #11975, #13043, .T. ) ;
#3717=AXIS2_PLACEMENT_3D ( 'NONE', #13489, #1362, #3867 ) ;
#3731=CIRCLE ( 'NONE', #11531, 1.999999999999991340 ) ;
#3733=AXIS2_PLACEMENT_3D ( 'NONE', #6759, #13185, #5901 ) ;
#3747=DIRECTION ( 'NONE',  ( 0.000000000000000000, 0.000000000000000000, 1.000000000000000000 ) ) ;
#3761=DIRECTION ( 'NONE',  ( -0.000000000000000000, 1.000000000000000000, -0.000000000000000000 ) ) ;
#3766=CARTESIAN_POINT ( 'NONE',  ( 4.599650328638321461, 8.500000000000001776, 7.878124499050794149 ) ) ;
#3786=AXIS2_PLACEMENT_3D ( 'NONE', #1709, #1791, #10440 ) ;
#3787=ORIENTED_EDGE ( 'NONE', *, *, #10166, .T. ) ;
#3814=CARTESIAN_POINT ( 'NONE',  ( 16.08092853089229024, 4.500000000000000000, -9.237812082545193704 ) ) ;
#3820=AXIS2_PLACEMENT_3D ( 'NONE', #7220, #3006, #5266 ) ;
#3830=CARTESIAN_POINT ( 'NONE',  ( 0.04028432657539327000, 0.000000000000000000, -18.54539866546729243 ) ) ;
#3839=CARTESIAN_POINT ( 'NONE',  ( 0.000000000000000000, 4.500000000000000000, 0.000000000000000000 ) ) ;
#3845=CIRCLE ( 'NONE', #3396, 1.999999999999991340 ) ;
#3862=ORIENTED_EDGE ( 'NONE', *, *, #10846, .T. ) ;
#3867=DIRECTION ( 'NONE',  ( 0.000000000000000000, 0.000000000000000000, 1.000000000000000000 ) ) ;
#3950=DIRECTION ( 'NONE',  ( 0.000000000000000000, 0.000000000000000000, 1.000000000000000000 ) ) ;
#4000=ORIENTED_EDGE ( 'NONE', *, *, #13629, .F. ) ;
#4023=LINE ( 'NONE', #12338, #7981 ) ;
#4027=CYLINDRICAL_SURFACE ( 'NONE', #10527, 1.999999999999986233 ) ;
#4028=ADVANCED_FACE ( 'NONE', ( #11646 ), #11572, .F. ) ;
#4033=ADVANCED_FACE ( 'NONE', ( #4376 ), #12555, .T. ) ;
#4055=ORIENTED_EDGE ( 'NONE', *, *, #1353, .F. ) ;
#4101=PRODUCT_CONTEXT ( 'NONE', #9568, 'mechanical' ) ;
#4151=ORIENTED_EDGE ( 'NONE', *, *, #13482, .T. ) ;
#4156=LINE ( 'NONE', #6029, #6503 ) ;
#4159=DIRECTION ( 'NONE',  ( -0.000000000000000000, 1.000000000000000000, -0.000000000000000000 ) ) ;
#4168=DIRECTION ( 'NONE',  ( -0.000000000000000000, -1.000000000000000000, -0.000000000000000000 ) ) ;
#4226=DIRECTION ( 'NONE',  ( -0.000000000000000000, -1.000000000000000000, -0.000000000000000000 ) ) ;
#4292=VERTEX_POINT ( 'NONE', #6300 ) ;
#4305=FACE_OUTER_BOUND ( 'NONE', #985, .T. ) ;
#4339=ORIENTED_EDGE ( 'NONE', *, *, #10147, .F. ) ;
#4344=ORIENTED_EDGE ( 'NONE', *, *, #12872, .F. ) ;
#4374=CARTESIAN_POINT ( 'NONE',  ( 0.000000000000000000, 4.500000000000000000, -23.49999999999999645 ) ) ;
#4376=FACE_OUTER_BOUND ( 'NONE', #5298, .T. ) ;
#4392=CARTESIAN_POINT ( 'NONE',  ( -16.04064420431702942, 0.000000000000000000, -9.307586582922249718 ) ) ;
#4410=FACE_BOUND ( 'NONE', #6869, .T. ) ;
#4428=AXIS2_PLACEMENT_3D ( 'NONE', #10093, #5877, #9027 ) ;
#4431=CARTESIAN_POINT ( 'NONE',  ( -16.04064420431702942, 4.500000000000000000, -11.30758658292224084 ) ) ;
#4487=MANIFOLD_SOLID_BREP ( 'Cut-Extrude1', #565 ) ;
#4488=ORIENTED_EDGE ( 'NONE', *, *, #6099, .F. ) ;
#4506=CIRCLE ( 'NONE', #8308, 1.999999999999991340 ) ;
#4518=EDGE_CURVE ( 'NONE', #8191, #10863, #7823, .T. ) ;
#4536=EDGE_CURVE ( 'NONE', #2, #12520, #12575, .T. ) ;
#4541=CARTESIAN_POINT ( 'NONE',  ( 16.08092853089229024, 4.500000000000000000, -9.237812082545193704 ) ) ;
#4546=EDGE_LOOP ( 'NONE', ( #10484, #13145 ) ) ;
#4549=ORIENTED_EDGE ( 'NONE', *, *, #315, .T. ) ;
#4557=ORIENTED_EDGE ( 'NONE', *, *, #11880, .T. ) ;
#4564=CYLINDRICAL_SURFACE ( 'NONE', #1975, 1.999999999999991340 ) ;
#4576=ORIENTED_EDGE ( 'NONE', *, *, #6896, .T. ) ;
#4587=( NAMED_UNIT ( * ) PLANE_ANGLE_UNIT ( ) SI_UNIT ( $, .RADIAN. ) );
#4597=DIRECTION ( 'NONE',  ( 0.000000000000000000, 0.000000000000000000, 1.000000000000000000 ) ) ;
#4608=EDGE_CURVE ( 'NONE', #859, #4292, #3186, .T. ) ;
#4622=CARTESIAN_POINT ( 'NONE',  ( 0.000000000000000000, 4.500000000000000000, 0.000000000000000000 ) ) ;
#4631=CARTESIAN_POINT ( 'NONE',  ( 16.04064420431708982, 4.500000000000000000, 9.307586582922137808 ) ) ;
#4646=EDGE_CURVE ( 'NONE', #997, #11352, #7841, .T. ) ;
#4653=AXIS2_PLACEMENT_3D ( 'NONE', #7760, #7681, #12175 ) ;
#4662=ORIENTED_EDGE ( 'NONE', *, *, #9969, .F. ) ;
#4671=DIRECTION ( 'NONE',  ( 0.000000000000000000, 0.000000000000000000, 1.000000000000000000 ) ) ;
#4675=CARTESIAN_POINT ( 'NONE',  ( 16.04064420431708982, 4.500000000000000000, 9.307586582922137808 ) ) ;
#4679=CYLINDRICAL_SURFACE ( 'NONE', #1580, 1.999999999999986233 ) ;
#4693=DIRECTION ( 'NONE',  ( 0.000000000000000000, 1.000000000000000000, 0.000000000000000000 ) ) ;
#4713=ADVANCED_FACE ( 'NONE', ( #11097 ), #9980, .F. ) ;
#4758=PRESENTATION_STYLE_ASSIGNMENT (( #556 ) ) ;
#4764=DIRECTION ( 'NONE',  ( 0.000000000000000000, 0.000000000000000000, 1.000000000000000000 ) ) ;
#4772=ORIENTED_EDGE ( 'NONE', *, *, #6099, .T. ) ;
#4782=EDGE_CURVE ( 'NONE', #10863, #7611, #10127, .T. ) ;
#4792=DIRECTION ( 'NONE',  ( 0.000000000000000000, 0.000000000000000000, -1.000000000000000000 ) ) ;
#4796=CARTESIAN_POINT ( 'NONE',  ( -4.599650328638321461, 8.500000000000001776, -5.878124499050803919 ) ) ;
#4808=CIRCLE ( 'NONE', #10612, 1.999999999999986233 ) ;
#4818=CARTESIAN_POINT ( 'NONE',  ( 0.000000000000000000, 8.500000000000000000, 0.000000000000000000 ) ) ;
#4819=FILL_AREA_STYLE ('',( #499 ) ) ;
#4827=DIRECTION ( 'NONE',  ( 0.000000000000000000, 1.000000000000000000, 0.000000000000000000 ) ) ;
#4834=ADVANCED_FACE ( 'NONE', ( #7655, #481, #1309, #5567, #2662, #9857, #8856, #276, #12003, #3566 ), #12558, .F. ) ;
#4848=EDGE_CURVE ( 'NONE', #7299, #12691, #4506, .T. ) ;
#4861=FACE_OUTER_BOUND ( 'NONE', #10850, .T. ) ;
#4865=EDGE_CURVE ( 'NONE', #11975, #8119, #13211, .T. ) ;
#4938=VECTOR ( 'NONE', #3393, 1000.000000000000000 ) ;
#4983=AXIS2_PLACEMENT_3D ( 'NONE', #10267, #9343, #1662 ) ;
#4995=CYLINDRICAL_SURFACE ( 'NONE', #3786, 1.999999999999991340 ) ;
#5000=VERTEX_POINT ( 'NONE', #7480 ) ;
#5018=ADVANCED_FACE ( 'NONE', ( #11575 ), #12621, .F. ) ;
#5026=VECTOR ( 'NONE', #13624, 1000.000000000000000 ) ;
#5044=ORIENTED_EDGE ( 'NONE', *, *, #2342, .T. ) ;
#5047=ORIENTED_EDGE ( 'NONE', *, *, #6310, .F. ) ;
#5073=DIRECTION ( 'NONE',  ( 0.000000000000000000, 1.000000000000000000, 0.000000000000000000 ) ) ;
#5087=CARTESIAN_POINT ( 'NONE',  ( 0.000000000000000000, 8.500000000000000000, 0.000000000000000000 ) ) ;
#5096=EDGE_CURVE ( 'NONE', #12408, #11864, #6293, .T. ) ;
#5188=EDGE_CURVE ( 'NONE', #10557, #4292, #11981, .T. ) ;
#5195=DIRECTION ( 'NONE',  ( -0.000000000000000000, 1.000000000000000000, -0.000000000000000000 ) ) ;
#5210=DIRECTION ( 'NONE',  ( 0.000000000000000000, 0.000000000000000000, 1.000000000000000000 ) ) ;
#5223=DIRECTION ( 'NONE',  ( 0.000000000000000000, 1.000000000000000000, 0.000000000000000000 ) ) ;
#5225=DIRECTION ( 'NONE',  ( 0.000000000000000000, 1.000000000000000000, 0.000000000000000000 ) ) ;
#5237=LINE ( 'NONE', #11735, #5026 ) ;
#5239=CARTESIAN_POINT ( 'NONE',  ( 4.599650328638321461, 8.500000000000001776, 9.878124499050784380 ) ) ;
#5247=ORIENTED_EDGE ( 'NONE', *, *, #7641, .F. ) ;
#5266=DIRECTION ( 'NONE',  ( 0.000000000000000000, 0.000000000000000000, -1.000000000000000000 ) ) ;
#5269=DIRECTION ( 'NONE',  ( 0.000000000000000000, 0.000000000000000000, 1.000000000000000000 ) ) ;
#5287=EDGE_CURVE ( 'NONE', #9802, #7749, #2083, .T. ) ;
#5298=EDGE_LOOP ( 'NONE', ( #10558, #13361, #13222, #9460 ) ) ;
#5304=CARTESIAN_POINT ( 'NONE',  ( 4.599650328638321461, 8.500000000000000000, 5.878124499050807472 ) ) ;
#5306=CARTESIAN_POINT ( 'NONE',  ( 4.599650328638321461, 0.000000000000000000, 7.878124499050794149 ) ) ;
#5312=AXIS2_PLACEMENT_3D ( 'NONE', #7225, #5073, #8297 ) ;
#5328=CARTESIAN_POINT ( 'NONE',  ( 0.000000000000000000, -17.50000000000000000, 0.000000000000000000 ) ) ;
#5367=VERTEX_POINT ( 'NONE', #1922 ) ;
#5408=CARTESIAN_POINT ( 'NONE',  ( 16.08092853089229024, 4.500000000000000000, -9.237812082545193704 ) ) ;
#5417=EDGE_CURVE ( 'NONE', #8947, #3062, #8764, .T. ) ;
#5447=APPLICATION_CONTEXT ( 'automotive_design' ) ;
#5450=EDGE_LOOP ( 'NONE', ( #6834, #6405, #5673, #11515 ) ) ;
#5468=VERTEX_POINT ( 'NONE', #8971 ) ;
#5498=EDGE_CURVE ( 'NONE', #6848, #859, #7542, .T. ) ;
#5510=EDGE_CURVE ( 'NONE', #6605, #172, #6761, .T. ) ;
#5511=DIRECTION ( 'NONE',  ( 0.000000000000000000, 1.000000000000000000, 0.000000000000000000 ) ) ;
#5547=ORIENTED_EDGE ( 'NONE', *, *, #10218, .T. ) ;
#5550=DIRECTION ( 'NONE',  ( 0.000000000000000000, 1.000000000000000000, 0.000000000000000000 ) ) ;
#5564=CARTESIAN_POINT ( 'NONE',  ( -16.08092853089235774, 4.500000000000000000, 11.23781208254507824 ) ) ;
#5567=FACE_BOUND ( 'NONE', #12158, .T. ) ;
#5599=EDGE_CURVE ( 'NONE', #3420, #5468, #7195, .T. ) ;
#5600=CARTESIAN_POINT ( 'NONE',  ( -0.04028432657539327000, 4.500000000000000000, 18.54539866546729243 ) ) ;
#5671=AXIS2_PLACEMENT_3D ( 'NONE', #12103, #4827, #5869 ) ;
#5673=ORIENTED_EDGE ( 'NONE', *, *, #1286, .T. ) ;
#5736=CIRCLE ( 'NONE', #12224, 1.999999999999989564 ) ;
#5740=ADVANCED_BREP_SHAPE_REPRESENTATION ( '', ( #4487, #6434 ), #10026 ) ;
#5760=CIRCLE ( 'NONE', #3325, 1.999999999999989564 ) ;
#5808=EDGE_LOOP ( 'NONE', ( #8436, #4772 ) ) ;
#5822=VECTOR ( 'NONE', #13609, 1000.000000000000000 ) ;
#5835=EDGE_LOOP ( 'NONE', ( #10374, #5247, #13510, #10923 ) ) ;
#5858=CARTESIAN_POINT ( 'NONE',  ( 0.04028432657539327000, 4.500000000000000000, -18.54539866546729243 ) ) ;
#5869=DIRECTION ( 'NONE',  ( 0.000000000000000000, 0.000000000000000000, 1.000000000000000000 ) ) ;
#5877=DIRECTION ( 'NONE',  ( 0.000000000000000000, 1.000000000000000000, 0.000000000000000000 ) ) ;
#5878=FACE_OUTER_BOUND ( 'NONE', #12236, .T. ) ;
#5884=ORIENTED_EDGE ( 'NONE', *, *, #7641, .T. ) ;
#5901=DIRECTION ( 'NONE',  ( 0.000000000000000000, 0.000000000000000000, 1.000000000000000000 ) ) ;
#5909=DIRECTION ( 'NONE',  ( -0.000000000000000000, 1.000000000000000000, -0.000000000000000000 ) ) ;
#5918=AXIS2_PLACEMENT_3D ( 'NONE', #12062, #2522, #6755 ) ;
#5946=ORIENTED_EDGE ( 'NONE', *, *, #6310, .T. ) ;
#5962=AXIS2_PLACEMENT_3D ( 'NONE', #4541, #12004, #2463 ) ;
#5973=CYLINDRICAL_SURFACE ( 'NONE', #8667, 23.49999999999999645 ) ;
#5982=PRODUCT_DEFINITION_CONTEXT ( 'detailed design', #5447, 'design' ) ;
#5985=VERTEX_POINT ( 'NONE', #11305 ) ;
#6011=DIRECTION ( 'NONE',  ( 0.000000000000000000, 0.000000000000000000, 1.000000000000000000 ) ) ;
#6029=CARTESIAN_POINT ( 'NONE',  ( -0.04028432657539302714, 4.500000000000000000, 16.54539866546730309 ) ) ;
#6038=AXIS2_PLACEMENT_3D ( 'NONE', #11923, #5550, #9753 ) ;
#6049=EDGE_CURVE ( 'NONE', #3062, #8947, #1873, .T. ) ;
#6059=ORIENTED_EDGE ( 'NONE', *, *, #4646, .F. ) ;
#6085=CARTESIAN_POINT ( 'NONE',  ( 2.877919977996279531E-15, 0.000000000000000000, 23.49999999999999645 ) ) ;
#6099=EDGE_CURVE ( 'NONE', #10148, #2, #7648, .T. ) ;
#6106=ORIENTED_EDGE ( 'NONE', *, *, #7825, .T. ) ;
#6118=UNCERTAINTY_MEASURE_WITH_UNIT (LENGTH_MEASURE( 1.000000000000000082E-05 ), #9964, 'distance_accuracy_value', 'NONE');
#6121=ORIENTED_EDGE ( 'NONE', *, *, #5287, .F. ) ;
#6123=ORIENTED_EDGE ( 'NONE', *, *, #11591, .T. ) ;
#6129=DIRECTION ( 'NONE',  ( 0.000000000000000000, 1.000000000000000000, 0.000000000000000000 ) ) ;
#6134=CARTESIAN_POINT ( 'NONE',  ( -16.04064420431702942, 4.500000000000000000, -7.307586582922255047 ) ) ;
#6179=DIRECTION ( 'NONE',  ( 0.000000000000000000, 0.000000000000000000, 1.000000000000000000 ) ) ;
#6192=ORIENTED_EDGE ( 'NONE', *, *, #13085, .F. ) ;
#6257=DIRECTION ( 'NONE',  ( -0.000000000000000000, 1.000000000000000000, -0.000000000000000000 ) ) ;
#6286=AXIS2_PLACEMENT_3D ( 'NONE', #3285, #12708, #978 ) ;
#6293=CIRCLE ( 'NONE', #12988, 1.999999999999991340 ) ;
#6299=LINE ( 'NONE', #5304, #13174 ) ;
#6300=CARTESIAN_POINT ( 'NONE',  ( -16.08092853089235774, 4.500000000000000000, 7.237812082545088899 ) ) ;
#6308=VECTOR ( 'NONE', #2576, 1000.000000000000000 ) ;
#6310=EDGE_CURVE ( 'NONE', #6705, #13129, #9367, .T. ) ;
#6314=VECTOR ( 'NONE', #13153, 1000.000000000000000 ) ;
#6315=ORIENTED_EDGE ( 'NONE', *, *, #11973, .F. ) ;
#6348=DIRECTION ( 'NONE',  ( 0.000000000000000000, 1.000000000000000000, 0.000000000000000000 ) ) ;
#6371=ORIENTED_EDGE ( 'NONE', *, *, #5599, .T. ) ;
#6405=ORIENTED_EDGE ( 'NONE', *, *, #1353, .T. ) ;
#6413=CARTESIAN_POINT ( 'NONE',  ( 7.347880794884120722E-16, 8.500000000000000000, -6.000000000000000888 ) ) ;
#6434=AXIS2_PLACEMENT_3D ( 'NONE', #11654, #12825, #11856 ) ;
#6438=AXIS2_PLACEMENT_3D ( 'NONE', #13493, #1626, #6011 ) ;
#6465=DIRECTION ( 'NONE',  ( -0.000000000000000000, 1.000000000000000000, -0.000000000000000000 ) ) ;
#6490=ADVANCED_FACE ( 'NONE', ( #4861 ), #4995, .F. ) ;
#6495=ADVANCED_FACE ( 'NONE', ( #12402 ), #1862, .F. ) ;
#6503=VECTOR ( 'NONE', #5195, 1000.000000000000000 ) ;
#6507=LINE ( 'NONE', #10991, #7772 ) ;
#6545=ORIENTED_EDGE ( 'NONE', *, *, #1790, .T. ) ;
#6554=DIRECTION ( 'NONE',  ( -0.000000000000000000, 1.000000000000000000, -0.000000000000000000 ) ) ;
#6605=VERTEX_POINT ( 'NONE', #8475 ) ;
#6611=ORIENTED_EDGE ( 'NONE', *, *, #2777, .T. ) ;
#6640=ADVANCED_FACE ( 'NONE', ( #4305 ), #2145, .F. ) ;
#6666=DIRECTION ( 'NONE',  ( -0.000000000000000000, 1.000000000000000000, -0.000000000000000000 ) ) ;
#6683=ORIENTED_EDGE ( 'NONE', *, *, #8598, .F. ) ;
#6694=LINE ( 'NONE', #11609, #12730 ) ;
#6705=VERTEX_POINT ( 'NONE', #13653 ) ;
#6717=FACE_OUTER_BOUND ( 'NONE', #12735, .T. ) ;
#6755=DIRECTION ( 'NONE',  ( 0.000000000000000000, 0.000000000000000000, 1.000000000000000000 ) ) ;
#6758=DIRECTION ( 'NONE',  ( -0.000000000000000000, 1.000000000000000000, -0.000000000000000000 ) ) ;
#6759=CARTESIAN_POINT ( 'NONE',  ( -16.08092853089235774, 4.500000000000000000, 9.237812082545083570 ) ) ;
#6761=CIRCLE ( 'NONE', #7404, 23.49999999999999645 ) ;
#6779=FACE_BOUND ( 'NONE', #13161, .T. ) ;
#6783=VERTEX_POINT ( 'NONE', #1424 ) ;
#6834=ORIENTED_EDGE ( 'NONE', *, *, #5096, .F. ) ;
#6838=SURFACE_STYLE_FILL_AREA ( #4819 ) ;
#6848=VERTEX_POINT ( 'NONE', #6860 ) ;
#6860=CARTESIAN_POINT ( 'NONE',  ( -16.08092853089235774, 0.000000000000000000, 11.23781208254507469 ) ) ;
#6866=LINE ( 'NONE', #7774, #11075 ) ;
#6869=EDGE_LOOP ( 'NONE', ( #1011, #1996 ) ) ;
#6871=DIRECTION ( 'NONE',  ( 0.000000000000000000, 0.000000000000000000, 1.000000000000000000 ) ) ;
#6872=VECTOR ( 'NONE', #4226, 1000.000000000000000 ) ;
#6875=DIRECTION ( 'NONE',  ( 0.000000000000000000, 0.000000000000000000, 1.000000000000000000 ) ) ;
#6876=FACE_OUTER_BOUND ( 'NONE', #2292, .T. ) ;
#6881=VECTOR ( 'NONE', #13241, 1000.000000000000000 ) ;
#6889=DIRECTION ( 'NONE',  ( 0.000000000000000000, 1.000000000000000000, 0.000000000000000000 ) ) ;
#6896=EDGE_CURVE ( 'NONE', #4292, #859, #11159, .T. ) ;
#6915=AXIS2_PLACEMENT_3D ( 'NONE', #2984, #11273, #785 ) ;
#6920=ORIENTED_EDGE ( 'NONE', *, *, #5498, .F. ) ;
#6938=ORIENTED_EDGE ( 'NONE', *, *, #400, .F. ) ;
#7033=ORIENTED_EDGE ( 'NONE', *, *, #4782, .F. ) ;
#7077=DIRECTION ( 'NONE',  ( -0.000000000000000000, 1.000000000000000000, -0.000000000000000000 ) ) ;
#7099=CIRCLE ( 'NONE', #9112, 1.999999999999986233 ) ;
#7141=EDGE_LOOP ( 'NONE', ( #6192, #9924, #4576, #6920 ) ) ;
#7156=STYLED_ITEM ( 'NONE', ( #4758 ), #4487 ) ;
#7169=CARTESIAN_POINT ( 'NONE',  ( 0.000000000000000000, 0.000000000000000000, 0.000000000000000000 ) ) ;
#7194=DIRECTION ( 'NONE',  ( -0.000000000000000000, 1.000000000000000000, -0.000000000000000000 ) ) ;
#7195=CIRCLE ( 'NONE', #9220, 1.999999999999994893 ) ;
#7204=ORIENTED_EDGE ( 'NONE', *, *, #820, .T. ) ;
#7213=ADVANCED_FACE ( 'NONE', ( #9795, #10913, #6779, #11051, #1470, #9874, #4410, #6717 ), #13066, .T. ) ;
#7220=CARTESIAN_POINT ( 'NONE',  ( 0.000000000000000000, 8.500000000000000000, 0.000000000000000000 ) ) ;
#7221=CARTESIAN_POINT ( 'NONE',  ( -0.04028432657539302714, 4.500000000000000000, 16.54539866546729954 ) ) ;
#7223=CARTESIAN_POINT ( 'NONE',  ( 16.08092853089229024, 0.000000000000000000, -9.237812082545193704 ) ) ;
#7225=CARTESIAN_POINT ( 'NONE',  ( 0.000000000000000000, 4.500000000000000000, 0.000000000000000000 ) ) ;
#7261=EDGE_LOOP ( 'NONE', ( #3862, #10431 ) ) ;
#7279=CARTESIAN_POINT ( 'NONE',  ( 0.04028432657539327000, 0.000000000000000000, -16.54539866546730309 ) ) ;
#7284=AXIS2_PLACEMENT_3D ( 'NONE', #13026, #11979, #6871 ) ;
#7286=CARTESIAN_POINT ( 'NONE',  ( -4.599650328638321461, 8.500000000000000000, -7.878124499050794149 ) ) ;
#7299=VERTEX_POINT ( 'NONE', #7745 ) ;
#7304=AXIS2_PLACEMENT_3D ( 'NONE', #3766, #344, #12079 ) ;
#7383=AXIS2_PLACEMENT_3D ( 'NONE', #7286, #13789, #1087 ) ;
#7385=EDGE_LOOP ( 'NONE', ( #9699, #6106 ) ) ;
#7402=ORIENTED_EDGE ( 'NONE', *, *, #4608, .F. ) ;
#7403=EDGE_CURVE ( 'NONE', #10469, #7611, #9037, .T. ) ;
#7404=AXIS2_PLACEMENT_3D ( 'NONE', #11830, #13013, #13081 ) ;
#7410=CARTESIAN_POINT ( 'NONE',  ( -16.08092853089235774, 0.000000000000000000, 9.237812082545083570 ) ) ;
#7462=EDGE_LOOP ( 'NONE', ( #1363, #9847 ) ) ;
#7465=DIRECTION ( 'NONE',  ( 0.000000000000000000, 0.000000000000000000, 1.000000000000000000 ) ) ;
#7480=CARTESIAN_POINT ( 'NONE',  ( 0.000000000000000000, 8.500000000000000000, 6.000000000000000888 ) ) ;
#7497=PRODUCT_DEFINITION_SHAPE ( 'NONE', 'NONE',  #738 ) ;
#7511=CIRCLE ( 'NONE', #4428, 1.999999999999991340 ) ;
#7517=CARTESIAN_POINT ( 'NONE',  ( 16.08092853089229024, 0.000000000000000000, -9.237812082545193704 ) ) ;
#7528=ORIENTED_EDGE ( 'NONE', *, *, #9916, .F. ) ;
#7532=CARTESIAN_POINT ( 'NONE',  ( 0.000000000000000000, 4.500000000000000000, -13.50000000000000000 ) ) ;
#7541=AXIS2_PLACEMENT_3D ( 'NONE', #4622, #5511, #2341 ) ;
#7542=LINE ( 'NONE', #8683, #6314 ) ;
#7562=CARTESIAN_POINT ( 'NONE',  ( 16.08092853089229024, 0.000000000000000000, -11.23781208254518660 ) ) ;
#7579=EDGE_LOOP ( 'NONE', ( #7402, #8606 ) ) ;
#7596=COLOUR_RGB ( '', 0.40784314, 0.44705882, 0.49803922) ;
#7607=EDGE_LOOP ( 'NONE', ( #699, #6059, #4557, #6371 ) ) ;
#7611=VERTEX_POINT ( 'NONE', #7532 ) ;
#7615=ORIENTED_EDGE ( 'NONE', *, *, #11566, .F. ) ;
#7628=PRODUCT ( 'Flange', 'Flange', '', ( #4101 ) ) ;
#7641=EDGE_CURVE ( 'NONE', #2149, #380, #10372, .T. ) ;
#7643=DIRECTION ( 'NONE',  ( 0.000000000000000000, 1.000000000000000000, 0.000000000000000000 ) ) ;
#7648=CIRCLE ( 'NONE', #4983, 1.999999999999991340 ) ;
#7651=CARTESIAN_POINT ( 'NONE',  ( -4.599650328638321461, 8.500000000000000000, -9.878124499050780827 ) ) ;
#7655=FACE_BOUND ( 'NONE', #1339, .T. ) ;
#7674=AXIS2_PLACEMENT_3D ( 'NONE', #11321, #1751, #4764 ) ;
#7681=DIRECTION ( 'NONE',  ( 0.000000000000000000, 1.000000000000000000, 0.000000000000000000 ) ) ;
#7697=ORIENTED_EDGE ( 'NONE', *, *, #2415, .F. ) ;
#7720=DIRECTION ( 'NONE',  ( 0.000000000000000000, 0.000000000000000000, 1.000000000000000000 ) ) ;
#7721=CARTESIAN_POINT ( 'NONE',  ( -16.04064420431702942, 0.000000000000000000, -7.307586582922258600 ) ) ;
#7723=CARTESIAN_POINT ( 'NONE',  ( -0.04028432657539302714, 0.000000000000000000, 16.54539866546730309 ) ) ;
#7728=CARTESIAN_POINT ( 'NONE',  ( 16.04064420431708982, 4.500000000000000000, 7.307586582922145801 ) ) ;
#7739=CIRCLE ( 'NONE', #3090, 1.999999999999991340 ) ;
#7740=CARTESIAN_POINT ( 'NONE',  ( 0.000000000000000000, 8.500000000000000000, 0.000000000000000000 ) ) ;
#7745=CARTESIAN_POINT ( 'NONE',  ( 16.08092853089229024, 0.000000000000000000, -7.237812082545202585 ) ) ;
#7749=VERTEX_POINT ( 'NONE', #13125 ) ;
#7758=EDGE_LOOP ( 'NONE', ( #11072, #12542 ) ) ;
#7760=CARTESIAN_POINT ( 'NONE',  ( 16.04064420431708982, 0.000000000000000000, 9.307586582922137808 ) ) ;
#7772=VECTOR ( 'NONE', #2475, 1000.000000000000000 ) ;
#7774=CARTESIAN_POINT ( 'NONE',  ( 4.599650328638321461, 8.500000000000000000, 9.878124499050780827 ) ) ;
#7787=CYLINDRICAL_SURFACE ( 'NONE', #5918, 1.999999999999991340 ) ;
#7815=CIRCLE ( 'NONE', #9392, 13.50000000000000000 ) ;
#7823=CIRCLE ( 'NONE', #12967, 13.50000000000000000 ) ;
#7825=EDGE_CURVE ( 'NONE', #5985, #6783, #4808, .T. ) ;
#7833=DIRECTION ( 'NONE',  ( 0.000000000000000000, 0.000000000000000000, 1.000000000000000000 ) ) ;
#7841=CIRCLE ( 'NONE', #11210, 1.999999999999991340 ) ;
#7853=CYLINDRICAL_SURFACE ( 'NONE', #9862, 13.50000000000000000 ) ;
#7854=DIRECTION ( 'NONE',  ( 0.000000000000000000, 0.000000000000000000, 1.000000000000000000 ) ) ;
#7855=SHAPE_REPRESENTATION_RELATIONSHIP ( 'NONE' , 'NONE' ,  #10413, #5740 ) ;
#7863=DIRECTION ( 'NONE',  ( -0.000000000000000000, 1.000000000000000000, -0.000000000000000000 ) ) ;
#7869=CARTESIAN_POINT ( 'NONE',  ( -16.08092853089235774, 0.000000000000000000, 7.237812082545092451 ) ) ;
#7959=EDGE_LOOP ( 'NONE', ( #7204, #10467 ) ) ;
#7981=VECTOR ( 'NONE', #2785, 1000.000000000000000 ) ;
#8008=DIRECTION ( 'NONE',  ( 0.000000000000000000, 0.000000000000000000, 1.000000000000000000 ) ) ;
#8049=CARTESIAN_POINT ( 'NONE',  ( 7.347880794884120722E-16, -17.50000000000000000, -6.000000000000000888 ) ) ;
#8050=DIRECTION ( 'NONE',  ( 0.000000000000000000, 0.000000000000000000, 1.000000000000000000 ) ) ;
#8096=ORIENTED_EDGE ( 'NONE', *, *, #12274, .F. ) ;
#8097=ORIENTED_EDGE ( 'NONE', *, *, #5599, .F. ) ;
#8119=VERTEX_POINT ( 'NONE', #4796 ) ;
#8122=CYLINDRICAL_SURFACE ( 'NONE', #6438, 1.999999999999991340 ) ;
#8145=CARTESIAN_POINT ( 'NONE',  ( -16.04064420431702942, 4.500000000000000000, -9.307586582922249718 ) ) ;
#8147=CARTESIAN_POINT ( 'NONE',  ( -4.599650328638321461, 8.500000000000001776, -7.878124499050794149 ) ) ;
#8151=CARTESIAN_POINT ( 'NONE',  ( 4.599650328638321461, 8.500000000000000000, 7.878124499050794149 ) ) ;
#8191=VERTEX_POINT ( 'NONE', #2454 ) ;
#8206=VERTEX_POINT ( 'NONE', #333 ) ;
#8262=ADVANCED_FACE ( 'NONE', ( #13104 ), #7787, .F. ) ;
#8297=DIRECTION ( 'NONE',  ( 0.000000000000000000, 0.000000000000000000, 1.000000000000000000 ) ) ;
#8308=AXIS2_PLACEMENT_3D ( 'NONE', #7223, #9339, #6179 ) ;
#8348=SHAPE_DEFINITION_REPRESENTATION ( #7497, #10413 ) ;
#8377=DIRECTION ( 'NONE',  ( 0.000000000000000000, 0.000000000000000000, 1.000000000000000000 ) ) ;
#8407=DIRECTION ( 'NONE',  ( 0.000000000000000000, 0.000000000000000000, 1.000000000000000000 ) ) ;
#8418=ORIENTED_EDGE ( 'NONE', *, *, #12862, .F. ) ;
#8436=ORIENTED_EDGE ( 'NONE', *, *, #66, .T. ) ;
#8446=PRODUCT_DEFINITION_FORMATION_WITH_SPECIFIED_SOURCE ( 'ANY', '', #7628, .NOT_KNOWN. ) ;
#8460=EDGE_CURVE ( 'NONE', #172, #8947, #11843, .T. ) ;
#8463=ORIENTED_EDGE ( 'NONE', *, *, #3698, .F. ) ;
#8475=CARTESIAN_POINT ( 'NONE',  ( 2.877919977996279531E-15, 4.500000000000000000, 23.49999999999999645 ) ) ;
#8476=VECTOR ( 'NONE', #6758, 1000.000000000000000 ) ;
#8480=VECTOR ( 'NONE', #7194, 1000.000000000000000 ) ;
#8544=CARTESIAN_POINT ( 'NONE',  ( 0.000000000000000000, 0.000000000000000000, 0.000000000000000000 ) ) ;
#8582=ORIENTED_EDGE ( 'NONE', *, *, #66, .F. ) ;
#8594=VECTOR ( 'NONE', #4168, 1000.000000000000000 ) ;
#8598=EDGE_CURVE ( 'NONE', #5367, #11674, #6866, .T. ) ;
#8603=ORIENTED_EDGE ( 'NONE', *, *, #5096, .T. ) ;
#8606=ORIENTED_EDGE ( 'NONE', *, *, #6896, .F. ) ;
#8627=AXIS2_PLACEMENT_3D ( 'NONE', #2733, #6889, #4597 ) ;
#8667=AXIS2_PLACEMENT_3D ( 'NONE', #3839, #12484, #2944 ) ;
#8670=ORIENTED_EDGE ( 'NONE', *, *, #10218, .F. ) ;
#8683=CARTESIAN_POINT ( 'NONE',  ( -16.08092853089235774, 4.500000000000000000, 11.23781208254507469 ) ) ;
#8721=DIRECTION ( 'NONE',  ( 0.000000000000000000, 0.000000000000000000, 1.000000000000000000 ) ) ;
#8738=ORIENTED_EDGE ( 'NONE', *, *, #7825, .F. ) ;
#8764=CIRCLE ( 'NONE', #2320, 23.49999999999999645 ) ;
#8765=ORIENTED_EDGE ( 'NONE', *, *, #9182, .T. ) ;
#8790=CARTESIAN_POINT ( 'NONE',  ( 0.000000000000000000, 8.500000000000000000, -13.50000000000000000 ) ) ;
#8801=CARTESIAN_POINT ( 'NONE',  ( 0.000000000000000000, 0.000000000000000000, -23.49999999999999645 ) ) ;
#8853=CARTESIAN_POINT ( 'NONE',  ( 16.08092853089229024, 4.500000000000000000, -9.237812082545193704 ) ) ;
#8856=FACE_BOUND ( 'NONE', #7261, .T. ) ;
#8881=AXIS2_PLACEMENT_3D ( 'NONE', #8853, #3563, #8927 ) ;
#8890=DIRECTION ( 'NONE',  ( -0.000000000000000000, 1.000000000000000000, -0.000000000000000000 ) ) ;
#8907=CARTESIAN_POINT ( 'NONE',  ( 16.08092853089229024, 4.500000000000000000, -7.237812082545199921 ) ) ;
#8927=DIRECTION ( 'NONE',  ( 0.000000000000000000, 0.000000000000000000, 1.000000000000000000 ) ) ;
#8947=VERTEX_POINT ( 'NONE', #8801 ) ;
#8948=EDGE_LOOP ( 'NONE', ( #2332, #9379, #10925, #6683 ) ) ;
#8968=DIRECTION ( 'NONE',  ( 0.000000000000000000, 0.000000000000000000, 1.000000000000000000 ) ) ;
#8971=CARTESIAN_POINT ( 'NONE',  ( -16.04064420431702942, 4.500000000000000000, -11.30758658292224439 ) ) ;
#9027=DIRECTION ( 'NONE',  ( 0.000000000000000000, 0.000000000000000000, 1.000000000000000000 ) ) ;
#9037=CIRCLE ( 'NONE', #7674, 13.50000000000000000 ) ;
#9066=ORIENTED_EDGE ( 'NONE', *, *, #5510, .T. ) ;
#9073=CARTESIAN_POINT ( 'NONE',  ( -4.599650328638321461, 8.500000000000001776, -9.878124499050784380 ) ) ;
#9099=CIRCLE ( 'NONE', #4653, 1.999999999999991340 ) ;
#9111=CARTESIAN_POINT ( 'NONE',  ( -0.04028432657539327000, 4.500000000000000000, 20.54539866546728888 ) ) ;
#9112=AXIS2_PLACEMENT_3D ( 'NONE', #5306, #12591, #3182 ) ;
#9139=DIRECTION ( 'NONE',  ( 0.000000000000000000, 1.000000000000000000, 0.000000000000000000 ) ) ;
#9151=ORIENTED_EDGE ( 'NONE', *, *, #4536, .T. ) ;
#9160=AXIS2_PLACEMENT_3D ( 'NONE', #399, #336, #4671 ) ;
#9182=EDGE_CURVE ( 'NONE', #5000, #13550, #12199, .T. ) ;
#9183=MECHANICAL_DESIGN_GEOMETRIC_PRESENTATION_REPRESENTATION('',(#7156),#486);
#9186=ORIENTED_EDGE ( 'NONE', *, *, #507, .T. ) ;
#9220=AXIS2_PLACEMENT_3D ( 'NONE', #2838, #1694, #8050 ) ;
#9238=EDGE_LOOP ( 'NONE', ( #8097, #4339 ) ) ;
#9257=DIRECTION ( 'NONE',  ( -0.000000000000000000, 1.000000000000000000, -0.000000000000000000 ) ) ;
#9269=ORIENTED_EDGE ( 'NONE', *, *, #1949, .F. ) ;
#9295=FACE_OUTER_BOUND ( 'NONE', #7607, .T. ) ;
#9339=DIRECTION ( 'NONE',  ( 0.000000000000000000, 1.000000000000000000, 0.000000000000000000 ) ) ;
#9340=CARTESIAN_POINT ( 'NONE',  ( 0.000000000000000000, 4.500000000000000000, 0.000000000000000000 ) ) ;
#9343=DIRECTION ( 'NONE',  ( 0.000000000000000000, 1.000000000000000000, 0.000000000000000000 ) ) ;
#9347=ADVANCED_FACE ( 'NONE', ( #12828 ), #11231, .F. ) ;
#9354=EDGE_LOOP ( 'NONE', ( #3657, #13716, #13007, #7528 ) ) ;
#9366=EDGE_CURVE ( 'NONE', #13129, #6705, #12205, .T. ) ;
#9367=CIRCLE ( 'NONE', #13365, 6.000000000000000888 ) ;
#9376=ORIENTED_EDGE ( 'NONE', *, *, #1949, .T. ) ;
#9379=ORIENTED_EDGE ( 'NONE', *, *, #400, .T. ) ;
#9392=AXIS2_PLACEMENT_3D ( 'NONE', #5087, #6348, #13608 ) ;
#9409=VERTEX_POINT ( 'NONE', #11155 ) ;
#9460=ORIENTED_EDGE ( 'NONE', *, *, #12563, .T. ) ;
#9463=DIRECTION ( 'NONE',  ( -0.000000000000000000, 1.000000000000000000, -0.000000000000000000 ) ) ;
#9468=CARTESIAN_POINT ( 'NONE',  ( -4.599650328638321461, 8.500000000000000000, -7.878124499050794149 ) ) ;
#9471=VERTEX_POINT ( 'NONE', #7221 ) ;
#9472=EDGE_CURVE ( 'NONE', #8191, #10469, #10530, .T. ) ;
#9553=AXIS2_PLACEMENT_3D ( 'NONE', #8145, #9463, #8008 ) ;
#9568=APPLICATION_CONTEXT ( 'automotive_design' ) ;
#9578=CARTESIAN_POINT ( 'NONE',  ( 1.653273178848926867E-15, 4.500000000000000000, 13.50000000000000000 ) ) ;
#9620=DIRECTION ( 'NONE',  ( 0.000000000000000000, 0.000000000000000000, 1.000000000000000000 ) ) ;
#9650=ORIENTED_EDGE ( 'NONE', *, *, #662, .T. ) ;
#9670=CARTESIAN_POINT ( 'NONE',  ( 2.877919977996279531E-15, 4.500000000000000000, 23.49999999999999645 ) ) ;
#9673=DIRECTION ( 'NONE',  ( 0.000000000000000000, 1.000000000000000000, 0.000000000000000000 ) ) ;
#9680=ORIENTED_EDGE ( 'NONE', *, *, #315, .F. ) ;
#9683=DIRECTION ( 'NONE',  ( 0.000000000000000000, 0.000000000000000000, 1.000000000000000000 ) ) ;
#9699=ORIENTED_EDGE ( 'NONE', *, *, #10649, .T. ) ;
#9719=DIRECTION ( 'NONE',  ( 0.000000000000000000, 0.000000000000000000, 1.000000000000000000 ) ) ;
#9739=AXIS2_PLACEMENT_3D ( 'NONE', #10400, #5223, #823 ) ;
#9753=DIRECTION ( 'NONE',  ( 0.000000000000000000, 0.000000000000000000, 1.000000000000000000 ) ) ;
#9771=CARTESIAN_POINT ( 'NONE',  ( 16.08092853089229024, 4.500000000000000000, -11.23781208254518660 ) ) ;
#9772=EDGE_CURVE ( 'NONE', #2628, #5367, #12883, .T. ) ;
#9795=FACE_BOUND ( 'NONE', #115, .T. ) ;
#9802=VERTEX_POINT ( 'NONE', #8907 ) ;
#9847=ORIENTED_EDGE ( 'NONE', *, *, #11591, .F. ) ;
#9857=FACE_BOUND ( 'NONE', #12333, .T. ) ;
#9862=AXIS2_PLACEMENT_3D ( 'NONE', #595, #2579, #4792 ) ;
#9874=FACE_BOUND ( 'NONE', #7462, .T. ) ;
#9880=VERTEX_POINT ( 'NONE', #9111 ) ;
#9886=CARTESIAN_POINT ( 'NONE',  ( -0.04028432657539327000, 4.500000000000000000, 18.54539866546729243 ) ) ;
#9916=EDGE_CURVE ( 'NONE', #7299, #9802, #4023, .T. ) ;
#9924=ORIENTED_EDGE ( 'NONE', *, *, #5188, .T. ) ;
#9942=CARTESIAN_POINT ( 'NONE',  ( 0.04028432657539351286, 0.000000000000000000, -20.54539866546728533 ) ) ;
#9964=( LENGTH_UNIT ( ) NAMED_UNIT ( * ) SI_UNIT ( .MILLI., .METRE. ) );
#9969=EDGE_CURVE ( 'NONE', #6605, #3062, #2206, .T. ) ;
#9975=FACE_OUTER_BOUND ( 'NONE', #8948, .T. ) ;
#9980=CYLINDRICAL_SURFACE ( 'NONE', #1376, 1.999999999999991340 ) ;
#9995=PLANE ( 'NONE',  #1803 ) ;
#10009=ORIENTED_EDGE ( 'NONE', *, *, #11566, .T. ) ;
#10026=( GEOMETRIC_REPRESENTATION_CONTEXT ( 3 ) GLOBAL_UNCERTAINTY_ASSIGNED_CONTEXT ( ( #6118 ) ) GLOBAL_UNIT_ASSIGNED_CONTEXT ( ( #9964, #4587, #10958 ) ) REPRESENTATION_CONTEXT ( 'NONE', 'WORKASPACE' ) );
#10031=CIRCLE ( 'NONE', #10690, 1.999999999999986233 ) ;
#10072=DIRECTION ( 'NONE',  ( 0.000000000000000000, 0.000000000000000000, 1.000000000000000000 ) ) ;
#10093=CARTESIAN_POINT ( 'NONE',  ( -0.04028432657539327000, 0.000000000000000000, 18.54539866546729243 ) ) ;
#10113=DIRECTION ( 'NONE',  ( -0.000000000000000000, 1.000000000000000000, -0.000000000000000000 ) ) ;
#10127=LINE ( 'NONE', #8790, #10757 ) ;
#10135=EDGE_LOOP ( 'NONE', ( #8096, #1849, #12067, #12035 ) ) ;
#10147=EDGE_CURVE ( 'NONE', #5468, #3420, #2440, .T. ) ;
#10148=VERTEX_POINT ( 'NONE', #9942 ) ;
#10160=CARTESIAN_POINT ( 'NONE',  ( 16.04064420431708982, 4.500000000000000000, 7.307586582922142249 ) ) ;
#10166=EDGE_CURVE ( 'NONE', #9880, #9471, #413, .T. ) ;
#10167=ORIENTED_EDGE ( 'NONE', *, *, #4848, .T. ) ;
#10207=CARTESIAN_POINT ( 'NONE',  ( 0.04028432657539327000, 4.500000000000000000, -16.54539866546730309 ) ) ;
#10218=EDGE_CURVE ( 'NONE', #380, #2149, #9099, .T. ) ;
#10239=AXIS2_PLACEMENT_3D ( 'NONE', #4631, #8890, #7833 ) ;
#10252=AXIS2_PLACEMENT_3D ( 'NONE', #1675, #2757, #624 ) ;
#10267=CARTESIAN_POINT ( 'NONE',  ( 0.04028432657539327000, 0.000000000000000000, -18.54539866546729243 ) ) ;
#10276=DIRECTION ( 'NONE',  ( 0.000000000000000000, -0.000000000000000000, 1.000000000000000000 ) ) ;
#10301=ADVANCED_FACE ( 'NONE', ( #5878 ), #8122, .F. ) ;
#10310=CARTESIAN_POINT ( 'NONE',  ( 4.599650328638321461, 0.000000000000000000, 5.878124499050807472 ) ) ;
#10372=CIRCLE ( 'NONE', #5671, 1.999999999999991340 ) ;
#10374=ORIENTED_EDGE ( 'NONE', *, *, #13482, .F. ) ;
#10382=CARTESIAN_POINT ( 'NONE',  ( 1.653273178848926867E-15, 8.500000000000000000, 13.50000000000000000 ) ) ;
#10385=CYLINDRICAL_SURFACE ( 'NONE', #13357, 23.49999999999999645 ) ;
#10400=CARTESIAN_POINT ( 'NONE',  ( 0.000000000000000000, 8.500000000000000000, 0.000000000000000000 ) ) ;
#10413=SHAPE_REPRESENTATION ( 'Flange', ( #6434 ), #10026 ) ;
#10431=ORIENTED_EDGE ( 'NONE', *, *, #13085, .T. ) ;
#10440=DIRECTION ( 'NONE',  ( 0.000000000000000000, 0.000000000000000000, 1.000000000000000000 ) ) ;
#10459=EDGE_CURVE ( 'NONE', #5367, #2628, #7099, .T. ) ;
#10467=ORIENTED_EDGE ( 'NONE', *, *, #4518, .T. ) ;
#10468=DIRECTION ( 'NONE',  ( 0.000000000000000000, 0.000000000000000000, 1.000000000000000000 ) ) ;
#10469=VERTEX_POINT ( 'NONE', #9578 ) ;
#10484=ORIENTED_EDGE ( 'NONE', *, *, #10459, .T. ) ;
#10510=ORIENTED_EDGE ( 'NONE', *, *, #1602, .F. ) ;
#10516=FACE_OUTER_BOUND ( 'NONE', #11958, .T. ) ;
#10527=AXIS2_PLACEMENT_3D ( 'NONE', #9468, #4159, #8407 ) ;
#10530=LINE ( 'NONE', #10382, #2419 ) ;
#10540=AXIS2_PLACEMENT_3D ( 'NONE', #3011, #12413, #746 ) ;
#10557=VERTEX_POINT ( 'NONE', #7869 ) ;
#10558=ORIENTED_EDGE ( 'NONE', *, *, #9472, .F. ) ;
#10571=EDGE_LOOP ( 'NONE', ( #5884, #5547 ) ) ;
#10593=CARTESIAN_POINT ( 'NONE',  ( 0.000000000000000000, 8.500000000000000000, -13.50000000000000000 ) ) ;
#10612=AXIS2_PLACEMENT_3D ( 'NONE', #11586, #2954, #10468 ) ;
#10621=EDGE_LOOP ( 'NONE', ( #1994, #6315 ) ) ;
#10639=CYLINDRICAL_SURFACE ( 'NONE', #9553, 1.999999999999991340 ) ;
#10649=EDGE_CURVE ( 'NONE', #6783, #5985, #10031, .T. ) ;
#10683=CIRCLE ( 'NONE', #11778, 1.999999999999994893 ) ;
#10690=AXIS2_PLACEMENT_3D ( 'NONE', #13316, #2532, #9719 ) ;
#10708=ORIENTED_EDGE ( 'NONE', *, *, #2342, .F. ) ;
#10721=DIRECTION ( 'NONE',  ( 0.000000000000000000, 0.000000000000000000, 1.000000000000000000 ) ) ;
#10745=CIRCLE ( 'NONE', #12531, 1.999999999999994893 ) ;
#10755=DIRECTION ( 'NONE',  ( -0.000000000000000000, 1.000000000000000000, -0.000000000000000000 ) ) ;
#10757=VECTOR ( 'NONE', #541, 1000.000000000000000 ) ;
#10773=AXIS2_PLACEMENT_3D ( 'NONE', #3814, #9257, #3950 ) ;
#10794=ADVANCED_FACE ( 'NONE', ( #2027 ), #10385, .T. ) ;
#10805=CARTESIAN_POINT ( 'NONE',  ( -0.04028432657539327000, 4.500000000000000000, 18.54539866546729243 ) ) ;
#10821=DIRECTION ( 'NONE',  ( -0.000000000000000000, 1.000000000000000000, -0.000000000000000000 ) ) ;
#10846=EDGE_CURVE ( 'NONE', #6848, #10557, #1776, .T. ) ;
#10850=EDGE_LOOP ( 'NONE', ( #4055, #7615, #3304, #3787 ) ) ;
#10853=DIRECTION ( 'NONE',  ( -0.000000000000000000, 1.000000000000000000, -0.000000000000000000 ) ) ;
#10863=VERTEX_POINT ( 'NONE', #10593 ) ;
#10866=ORIENTED_EDGE ( 'NONE', *, *, #4865, .T. ) ;
#10913=FACE_BOUND ( 'NONE', #2845, .T. ) ;
#10923=ORIENTED_EDGE ( 'NONE', *, *, #263, .T. ) ;
#10925=ORIENTED_EDGE ( 'NONE', *, *, #12872, .T. ) ;
#10958=( NAMED_UNIT ( * ) SI_UNIT ( $, .STERADIAN. ) SOLID_ANGLE_UNIT ( ) );
#10991=CARTESIAN_POINT ( 'NONE',  ( -16.04064420431702942, 4.500000000000000000, -7.307586582922258600 ) ) ;
#10999=ORIENTED_EDGE ( 'NONE', *, *, #11880, .F. ) ;
#11025=CARTESIAN_POINT ( 'NONE',  ( 0.000000000000000000, 0.000000000000000000, 0.000000000000000000 ) ) ;
#11029=ORIENTED_EDGE ( 'NONE', *, *, #8598, .T. ) ;
#11051=FACE_BOUND ( 'NONE', #7579, .T. ) ;
#11070=EDGE_LOOP ( 'NONE', ( #13146, #12549 ) ) ;
#11072=ORIENTED_EDGE ( 'NONE', *, *, #5417, .F. ) ;
#11073=ADVANCED_FACE ( 'NONE', ( #539 ), #338, .F. ) ;
#11075=VECTOR ( 'NONE', #6666, 1000.000000000000000 ) ;
#11093=CARTESIAN_POINT ( 'NONE',  ( -0.04028432657539327000, 4.500000000000000000, 20.54539866546728533 ) ) ;
#11097=FACE_OUTER_BOUND ( 'NONE', #1425, .T. ) ;
#11103=ADVANCED_FACE ( 'NONE', ( #1307 ), #3690, .F. ) ;
#11155=CARTESIAN_POINT ( 'NONE',  ( 16.04064420431708982, 4.500000000000000000, 11.30758658292213248 ) ) ;
#11159=CIRCLE ( 'NONE', #6915, 1.999999999999994893 ) ;
#11175=ADVANCED_FACE ( 'NONE', ( #402 ), #10639, .F. ) ;
#11178=FACE_BOUND ( 'NONE', #10621, .T. ) ;
#11179=( NAMED_UNIT ( * ) SI_UNIT ( $, .STERADIAN. ) SOLID_ANGLE_UNIT ( ) );
#11191=ORIENTED_EDGE ( 'NONE', *, *, #10846, .F. ) ;
#11205=CARTESIAN_POINT ( 'NONE',  ( -16.04064420431702942, 0.000000000000000000, -9.307586582922249718 ) ) ;
#11210=AXIS2_PLACEMENT_3D ( 'NONE', #4392, #5225, #8721 ) ;
#11231=CYLINDRICAL_SURFACE ( 'NONE', #3733, 1.999999999999991340 ) ;
#11238=FACE_OUTER_BOUND ( 'NONE', #13086, .T. ) ;
#11261=ORIENTED_EDGE ( 'NONE', *, *, #11562, .F. ) ;
#11273=DIRECTION ( 'NONE',  ( -0.000000000000000000, 1.000000000000000000, -0.000000000000000000 ) ) ;
#11301=FACE_OUTER_BOUND ( 'NONE', #301, .T. ) ;
#11305=CARTESIAN_POINT ( 'NONE',  ( -4.599650328638321461, 0.000000000000000000, -9.878124499050780827 ) ) ;
#11321=CARTESIAN_POINT ( 'NONE',  ( 0.000000000000000000, 4.500000000000000000, 0.000000000000000000 ) ) ;
#11352=VERTEX_POINT ( 'NONE', #13077 ) ;
#11376=ADVANCED_FACE ( 'NONE', ( #2351 ), #4564, .F. ) ;
#11388=CIRCLE ( 'NONE', #11611, 1.999999999999994893 ) ;
#11404=EDGE_LOOP ( 'NONE', ( #11816, #5047, #436, #8765 ) ) ;
#11417=ORIENTED_EDGE ( 'NONE', *, *, #10459, .F. ) ;
#11503=CARTESIAN_POINT ( 'NONE',  ( 0.04028432657539327000, 4.500000000000000000, -16.54539866546729954 ) ) ;
#11515=ORIENTED_EDGE ( 'NONE', *, *, #3666, .F. ) ;
#11531=AXIS2_PLACEMENT_3D ( 'NONE', #3830, #12879, #9683 ) ;
#11534=CARTESIAN_POINT ( 'NONE',  ( 0.04028432657539327000, 4.500000000000000000, -18.54539866546729243 ) ) ;
#11562=EDGE_CURVE ( 'NONE', #2919, #9409, #13127, .T. ) ;
#11564=AXIS2_PLACEMENT_3D ( 'NONE', #3226, #10821, #3161 ) ;
#11566=EDGE_CURVE ( 'NONE', #11864, #12408, #7511, .T. ) ;
#11572=CYLINDRICAL_SURFACE ( 'NONE', #1814, 1.999999999999991340 ) ;
#11575=FACE_OUTER_BOUND ( 'NONE', #724, .T. ) ;
#11586=CARTESIAN_POINT ( 'NONE',  ( -4.599650328638321461, 0.000000000000000000, -7.878124499050794149 ) ) ;
#11591=EDGE_CURVE ( 'NONE', #2653, #12520, #10683, .T. ) ;
#11609=CARTESIAN_POINT ( 'NONE',  ( 0.04028432657539351286, 4.500000000000000000, -20.54539866546728533 ) ) ;
#11611=AXIS2_PLACEMENT_3D ( 'NONE', #5858, #621, #10072 ) ;
#11643=CARTESIAN_POINT ( 'NONE',  ( 0.000000000000000000, 4.500000000000000000, -23.49999999999999645 ) ) ;
#11644=CIRCLE ( 'NONE', #1116, 1.999999999999991340 ) ;
#11646=FACE_OUTER_BOUND ( 'NONE', #10135, .T. ) ;
#11654=CARTESIAN_POINT ( 'NONE',  ( 0.000000000000000000, 0.000000000000000000, 0.000000000000000000 ) ) ;
#11674=VERTEX_POINT ( 'NONE', #5239 ) ;
#11712=CARTESIAN_POINT ( 'NONE',  ( -0.04028432657539327000, 0.000000000000000000, 18.54539866546729243 ) ) ;
#11735=CARTESIAN_POINT ( 'NONE',  ( -4.599650328638321461, 8.500000000000000000, -5.878124499050807472 ) ) ;
#11778=AXIS2_PLACEMENT_3D ( 'NONE', #11534, #780, #920 ) ;
#11779=CIRCLE ( 'NONE', #5962, 1.999999999999994893 ) ;
#11788=ORIENTED_EDGE ( 'NONE', *, *, #8460, .T. ) ;
#11816=ORIENTED_EDGE ( 'NONE', *, *, #1790, .F. ) ;
#11819=ORIENTED_EDGE ( 'NONE', *, *, #5417, .T. ) ;
#11830=CARTESIAN_POINT ( 'NONE',  ( 0.000000000000000000, 4.500000000000000000, 0.000000000000000000 ) ) ;
#11843=LINE ( 'NONE', #4374, #8594 ) ;
#11856=DIRECTION ( 'NONE',  ( 1.000000000000000000, 0.000000000000000000, 0.000000000000000000 ) ) ;
#11862=ORIENTED_EDGE ( 'NONE', *, *, #9969, .T. ) ;
#11864=VERTEX_POINT ( 'NONE', #7 ) ;
#11880=EDGE_CURVE ( 'NONE', #997, #3420, #6507, .T. ) ;
#11899=DIRECTION ( 'NONE',  ( -0.000000000000000000, 1.000000000000000000, -0.000000000000000000 ) ) ;
#11923=CARTESIAN_POINT ( 'NONE',  ( 0.000000000000000000, 4.500000000000000000, 0.000000000000000000 ) ) ;
#11931=CYLINDRICAL_SURFACE ( 'NONE', #9160, 1.999999999999986233 ) ;
#11938=DIRECTION ( 'NONE',  ( -0.000000000000000000, 1.000000000000000000, -0.000000000000000000 ) ) ;
#11942=LINE ( 'NONE', #7728, #2435 ) ;
#11958=EDGE_LOOP ( 'NONE', ( #8463, #1277, #4549, #13509 ) ) ;
#11968=DIRECTION ( 'NONE',  ( 0.000000000000000000, 1.000000000000000000, 0.000000000000000000 ) ) ;
#11973=EDGE_CURVE ( 'NONE', #13550, #5000, #3324, .T. ) ;
#11975=VERTEX_POINT ( 'NONE', #9073 ) ;
#11979=DIRECTION ( 'NONE',  ( 0.000000000000000000, 1.000000000000000000, 0.000000000000000000 ) ) ;
#11981=LINE ( 'NONE', #2442, #6308 ) ;
#12003=FACE_BOUND ( 'NONE', #5808, .T. ) ;
#12004=DIRECTION ( 'NONE',  ( -0.000000000000000000, 1.000000000000000000, -0.000000000000000000 ) ) ;
#12010=AXIS2_PLACEMENT_3D ( 'NONE', #2627, #10853, #2562 ) ;
#12035=ORIENTED_EDGE ( 'NONE', *, *, #5287, .T. ) ;
#12055=DIRECTION ( 'NONE',  ( 0.000000000000000000, 0.000000000000000000, 1.000000000000000000 ) ) ;
#12062=CARTESIAN_POINT ( 'NONE',  ( -16.08092853089235774, 4.500000000000000000, 9.237812082545083570 ) ) ;
#12067=ORIENTED_EDGE ( 'NONE', *, *, #9916, .T. ) ;
#12079=DIRECTION ( 'NONE',  ( 0.000000000000000000, 0.000000000000000000, 1.000000000000000000 ) ) ;
#12103=CARTESIAN_POINT ( 'NONE',  ( 16.04064420431708982, 0.000000000000000000, 9.307586582922137808 ) ) ;
#12130=DIRECTION ( 'NONE',  ( -0.000000000000000000, 1.000000000000000000, -0.000000000000000000 ) ) ;
#12158=EDGE_LOOP ( 'NONE', ( #10167, #9186 ) ) ;
#12175=DIRECTION ( 'NONE',  ( 0.000000000000000000, 0.000000000000000000, 1.000000000000000000 ) ) ;
#12182=EDGE_LOOP ( 'NONE', ( #4488, #9376, #6123, #1429 ) ) ;
#12199=CIRCLE ( 'NONE', #9739, 6.000000000000000888 ) ;
#12205=CIRCLE ( 'NONE', #8627, 6.000000000000000888 ) ;
#12224=AXIS2_PLACEMENT_3D ( 'NONE', #13097, #2645, #6875 ) ;
#12236=EDGE_LOOP ( 'NONE', ( #9269, #8582, #9151, #9650 ) ) ;
#12245=ORIENTED_EDGE ( 'NONE', *, *, #5498, .T. ) ;
#12274=EDGE_CURVE ( 'NONE', #12691, #7749, #12903, .T. ) ;
#12290=ADVANCED_FACE ( 'NONE', ( #12831 ), #2174, .F. ) ;
#12313=DIRECTION ( 'NONE',  ( -0.000000000000000000, 1.000000000000000000, -0.000000000000000000 ) ) ;
#12333=EDGE_LOOP ( 'NONE', ( #10009, #8603 ) ) ;
#12338=CARTESIAN_POINT ( 'NONE',  ( 16.08092853089229024, 4.500000000000000000, -7.237812082545202585 ) ) ;
#12356=DIRECTION ( 'NONE',  ( 0.000000000000000000, 0.000000000000000000, 1.000000000000000000 ) ) ;
#12402=FACE_OUTER_BOUND ( 'NONE', #5835, .T. ) ;
#12408=VERTEX_POINT ( 'NONE', #7723 ) ;
#12413=DIRECTION ( 'NONE',  ( 0.000000000000000000, 1.000000000000000000, 0.000000000000000000 ) ) ;
#12452=EDGE_CURVE ( 'NONE', #7749, #9802, #11779, .T. ) ;
#12484=DIRECTION ( 'NONE',  ( -0.000000000000000000, -1.000000000000000000, -0.000000000000000000 ) ) ;
#12497=ADVANCED_FACE ( 'NONE', ( #11301 ), #5973, .T. ) ;
#12498=ORIENTED_EDGE ( 'NONE', *, *, #13629, .T. ) ;
#12520=VERTEX_POINT ( 'NONE', #11503 ) ;
#12531=AXIS2_PLACEMENT_3D ( 'NONE', #10805, #6465, #5269 ) ;
#12542=ORIENTED_EDGE ( 'NONE', *, *, #6049, .F. ) ;
#12549=ORIENTED_EDGE ( 'NONE', *, *, #4865, .F. ) ;
#12555=CYLINDRICAL_SURFACE ( 'NONE', #3820, 13.50000000000000000 ) ;
#12558=PLANE ( 'NONE',  #10540 ) ;
#12563=EDGE_CURVE ( 'NONE', #7611, #10469, #861, .T. ) ;
#12575=LINE ( 'NONE', #10207, #5822 ) ;
#12591=DIRECTION ( 'NONE',  ( 0.000000000000000000, 1.000000000000000000, 0.000000000000000000 ) ) ;
#12619=DIRECTION ( 'NONE',  ( -0.000000000000000000, -1.000000000000000000, -0.000000000000000000 ) ) ;
#12621=CYLINDRICAL_SURFACE ( 'NONE', #7383, 1.999999999999986233 ) ;
#12623=DIRECTION ( 'NONE',  ( 0.000000000000000000, 0.000000000000000000, -1.000000000000000000 ) ) ;
#12636=ORIENTED_EDGE ( 'NONE', *, *, #7403, .T. ) ;
#12665=EDGE_LOOP ( 'NONE', ( #377, #11862, #2295, #1765 ) ) ;
#12691=VERTEX_POINT ( 'NONE', #7562 ) ;
#12708=DIRECTION ( 'NONE',  ( -0.000000000000000000, 1.000000000000000000, -0.000000000000000000 ) ) ;
#12730=VECTOR ( 'NONE', #10755, 1000.000000000000000 ) ;
#12735=EDGE_LOOP ( 'NONE', ( #5044, #9066 ) ) ;
#12825=DIRECTION ( 'NONE',  ( 0.000000000000000000, 0.000000000000000000, 1.000000000000000000 ) ) ;
#12828=FACE_OUTER_BOUND ( 'NONE', #7141, .T. ) ;
#12831=FACE_OUTER_BOUND ( 'NONE', #12182, .T. ) ;
#12853=EDGE_CURVE ( 'NONE', #8119, #11975, #5760, .T. ) ;
#12862=EDGE_CURVE ( 'NONE', #2149, #9409, #327, .T. ) ;
#12872=EDGE_CURVE ( 'NONE', #8206, #11674, #5736, .T. ) ;
#12879=DIRECTION ( 'NONE',  ( 0.000000000000000000, 1.000000000000000000, 0.000000000000000000 ) ) ;
#12883=CIRCLE ( 'NONE', #7284, 1.999999999999986233 ) ;
#12903=LINE ( 'NONE', #9771, #179 ) ;
#12967=AXIS2_PLACEMENT_3D ( 'NONE', #7740, #6129, #8377 ) ;
#12988=AXIS2_PLACEMENT_3D ( 'NONE', #11712, #43, #5210 ) ;
#13007=ORIENTED_EDGE ( 'NONE', *, *, #12452, .T. ) ;
#13013=DIRECTION ( 'NONE',  ( 0.000000000000000000, 1.000000000000000000, 0.000000000000000000 ) ) ;
#13026=CARTESIAN_POINT ( 'NONE',  ( 4.599650328638321461, 0.000000000000000000, 7.878124499050794149 ) ) ;
#13029=CARTESIAN_POINT ( 'NONE',  ( -16.08092853089235774, 0.000000000000000000, 9.237812082545083570 ) ) ;
#13043=LINE ( 'NONE', #7651, #3593 ) ;
#13066=PLANE ( 'NONE',  #7541 ) ;
#13077=CARTESIAN_POINT ( 'NONE',  ( -16.04064420431702942, 0.000000000000000000, -11.30758658292224084 ) ) ;
#13081=DIRECTION ( 'NONE',  ( 0.000000000000000000, 0.000000000000000000, 1.000000000000000000 ) ) ;
#13085=EDGE_CURVE ( 'NONE', #10557, #6848, #7739, .T. ) ;
#13086=EDGE_LOOP ( 'NONE', ( #6938, #11417, #11029, #12498 ) ) ;
#13097=CARTESIAN_POINT ( 'NONE',  ( 4.599650328638321461, 8.500000000000001776, 7.878124499050794149 ) ) ;
#13104=FACE_OUTER_BOUND ( 'NONE', #79, .T. ) ;
#13125=CARTESIAN_POINT ( 'NONE',  ( 16.08092853089229024, 4.500000000000000000, -11.23781208254518837 ) ) ;
#13127=CIRCLE ( 'NONE', #10239, 1.999999999999994893 ) ;
#13129=VERTEX_POINT ( 'NONE', #91 ) ;
#13145=ORIENTED_EDGE ( 'NONE', *, *, #9772, .T. ) ;
#13146=ORIENTED_EDGE ( 'NONE', *, *, #12853, .F. ) ;
#13153=DIRECTION ( 'NONE',  ( -0.000000000000000000, 1.000000000000000000, -0.000000000000000000 ) ) ;
#13161=EDGE_LOOP ( 'NONE', ( #1430, #3280 ) ) ;
#13174=VECTOR ( 'NONE', #13751, 1000.000000000000000 ) ;
#13185=DIRECTION ( 'NONE',  ( -0.000000000000000000, 1.000000000000000000, -0.000000000000000000 ) ) ;
#13211=CIRCLE ( 'NONE', #716, 1.999999999999989564 ) ;
#13222=ORIENTED_EDGE ( 'NONE', *, *, #4782, .T. ) ;
#13241=DIRECTION ( 'NONE',  ( -0.000000000000000000, 1.000000000000000000, -0.000000000000000000 ) ) ;
#13316=CARTESIAN_POINT ( 'NONE',  ( -4.599650328638321461, 0.000000000000000000, -7.878124499050794149 ) ) ;
#13333=AXIS2_PLACEMENT_3D ( 'NONE', #479, #1384, #7720 ) ;
#13357=AXIS2_PLACEMENT_3D ( 'NONE', #9340, #809, #12623 ) ;
#13361=ORIENTED_EDGE ( 'NONE', *, *, #820, .F. ) ;
#13365=AXIS2_PLACEMENT_3D ( 'NONE', #11025, #7643, #7854 ) ;
#13482=EDGE_CURVE ( 'NONE', #380, #2919, #11942, .T. ) ;
#13489=CARTESIAN_POINT ( 'NONE',  ( 16.04064420431708982, 4.500000000000000000, 9.307586582922137808 ) ) ;
#13493=CARTESIAN_POINT ( 'NONE',  ( 0.04028432657539327000, 4.500000000000000000, -18.54539866546729243 ) ) ;
#13509=ORIENTED_EDGE ( 'NONE', *, *, #12853, .T. ) ;
#13510=ORIENTED_EDGE ( 'NONE', *, *, #12862, .T. ) ;
#13550=VERTEX_POINT ( 'NONE', #6413 ) ;
#13570=CIRCLE ( 'NONE', #7304, 1.999999999999989564 ) ;
#13608=DIRECTION ( 'NONE',  ( 0.000000000000000000, 0.000000000000000000, 1.000000000000000000 ) ) ;
#13609=DIRECTION ( 'NONE',  ( -0.000000000000000000, 1.000000000000000000, -0.000000000000000000 ) ) ;
#13614=CARTESIAN_POINT ( 'NONE',  ( -16.04064420431702942, 4.500000000000000000, -9.307586582922249718 ) ) ;
#13624=DIRECTION ( 'NONE',  ( -0.000000000000000000, 1.000000000000000000, -0.000000000000000000 ) ) ;
#13629=EDGE_CURVE ( 'NONE', #11674, #8206, #13570, .T. ) ;
#13641=ORIENTED_EDGE ( 'NONE', *, *, #11973, .T. ) ;
#13653=CARTESIAN_POINT ( 'NONE',  ( 0.000000000000000000, 0.000000000000000000, 6.000000000000000888 ) ) ;
#13716=ORIENTED_EDGE ( 'NONE', *, *, #12274, .T. ) ;
#13751=DIRECTION ( 'NONE',  ( -0.000000000000000000, 1.000000000000000000, -0.000000000000000000 ) ) ;
#13789=DIRECTION ( 'NONE',  ( -0.000000000000000000, 1.000000000000000000, -0.000000000000000000 ) ) ;
ENDSEC;
END-ISO-10303-21;
